ISO-10303-21;
HEADER;
/* Generated by software containing ST-Developer
 * from STEP Tools, Inc. (www.steptools.com) 
 */

FILE_DESCRIPTION(
/* description */ ('Shaft runout checking stand'),
/* implementation_level */ '2;1');

FILE_NAME(
/* name */ 'Axle keeper (3).step',
/* time_stamp */ '2026-11-02T21:12:33-08:00',
/* author */ (''),
/* organization */ (''),
/* preprocessor_version */ 'ST-DEVELOPER v20.2',
/* originating_system */ 'Autodesk Translation Framework v15.17.0.0',
/* authorisation */ '');

FILE_SCHEMA (('AUTOMOTIVE_DESIGN { 1 0 10303 214 3 1 1 }'));
ENDSEC;

DATA;
#10=MECHANICAL_DESIGN_GEOMETRIC_PRESENTATION_REPRESENTATION('',(#484),#11748);
#398=SHAPE_REPRESENTATION_RELATIONSHIP('SRR','None',#11947,#441);
#441=ADVANCED_BREP_SHAPE_REPRESENTATION('',(#534),#11723);
#484=STYLED_ITEM('',(#12169),#534);
#534=MANIFOLD_SOLID_BREP('Body1',#6228);
#632=FACE_BOUND('',#1679,.T.);
#633=FACE_BOUND('',#1681,.T.);
#791=CIRCLE('',#7079,0.225);
#792=CIRCLE('',#7080,0.225);
#793=CIRCLE('',#7082,0.8);
#794=CIRCLE('',#7083,0.8);
#994=CYLINDRICAL_SURFACE('',#7078,0.225);
#995=CYLINDRICAL_SURFACE('',#7081,0.8);
#1238=FACE_OUTER_BOUND('',#1676,.T.);
#1239=FACE_OUTER_BOUND('',#1677,.T.);
#1240=FACE_OUTER_BOUND('',#1678,.T.);
#1241=FACE_OUTER_BOUND('',#1680,.T.);
#1676=EDGE_LOOP('',(#4968,#4969,#4970,#4971));
#1677=EDGE_LOOP('',(#4972,#4973,#4974,#4975));
#1678=EDGE_LOOP('',(#4976));
#1679=EDGE_LOOP('',(#4977));
#1680=EDGE_LOOP('',(#4978));
#1681=EDGE_LOOP('',(#4979));
#2205=LINE('',#10435,#2672);
#2206=LINE('',#10441,#2673);
#2672=VECTOR('',#8504,0.225);
#2673=VECTOR('',#8511,0.8);
#3111=VERTEX_POINT('',#10432);
#3112=VERTEX_POINT('',#10434);
#3113=VERTEX_POINT('',#10438);
#3114=VERTEX_POINT('',#10440);
#3770=EDGE_CURVE('',#3111,#3111,#791,.T.);
#3771=EDGE_CURVE('',#3111,#3112,#2205,.T.);
#3772=EDGE_CURVE('',#3112,#3112,#792,.T.);
#3773=EDGE_CURVE('',#3113,#3113,#793,.T.);
#3774=EDGE_CURVE('',#3113,#3114,#2206,.T.);
#3775=EDGE_CURVE('',#3114,#3114,#794,.T.);
#4968=ORIENTED_EDGE('',*,*,#3770,.F.);
#4969=ORIENTED_EDGE('',*,*,#3771,.T.);
#4970=ORIENTED_EDGE('',*,*,#3772,.T.);
#4971=ORIENTED_EDGE('',*,*,#3771,.F.);
#4972=ORIENTED_EDGE('',*,*,#3773,.F.);
#4973=ORIENTED_EDGE('',*,*,#3774,.T.);
#4974=ORIENTED_EDGE('',*,*,#3775,.T.);
#4975=ORIENTED_EDGE('',*,*,#3774,.F.);
#4976=ORIENTED_EDGE('',*,*,#3773,.T.);
#4977=ORIENTED_EDGE('',*,*,#3770,.T.);
#4978=ORIENTED_EDGE('',*,*,#3775,.F.);
#4979=ORIENTED_EDGE('',*,*,#3772,.F.);
#5744=PLANE('',#7084);
#5745=PLANE('',#7085);
#6038=ADVANCED_FACE('',(#1238),#994,.F.);
#6039=ADVANCED_FACE('',(#1239),#995,.T.);
#6040=ADVANCED_FACE('',(#1240,#632),#5744,.T.);
#6041=ADVANCED_FACE('',(#1241,#633),#5745,.F.);
#6228=CLOSED_SHELL('',(#6038,#6039,#6040,#6041));
#7077=AXIS2_PLACEMENT_3D('',#10430,#8498,#8499);
#7078=AXIS2_PLACEMENT_3D('',#10431,#8500,#8501);
#7079=AXIS2_PLACEMENT_3D('',#10433,#8502,#8503);
#7080=AXIS2_PLACEMENT_3D('',#10436,#8505,#8506);
#7081=AXIS2_PLACEMENT_3D('',#10437,#8507,#8508);
#7082=AXIS2_PLACEMENT_3D('',#10439,#8509,#8510);
#7083=AXIS2_PLACEMENT_3D('',#10442,#8512,#8513);
#7084=AXIS2_PLACEMENT_3D('',#10443,#8514,#8515);
#7085=AXIS2_PLACEMENT_3D('',#10444,#8516,#8517);
#8498=DIRECTION('axis',(0.,0.,1.));
#8499=DIRECTION('refdir',(1.,0.,0.));
#8500=DIRECTION('center_axis',(0.,1.,0.));
#8501=DIRECTION('ref_axis',(1.,0.,0.));
#8502=DIRECTION('center_axis',(0.,-1.,0.));
#8503=DIRECTION('ref_axis',(1.,0.,0.));
#8504=DIRECTION('',(0.,-1.,0.));
#8505=DIRECTION('center_axis',(0.,-1.,0.));
#8506=DIRECTION('ref_axis',(1.,0.,0.));
#8507=DIRECTION('center_axis',(0.,1.,0.));
#8508=DIRECTION('ref_axis',(1.,0.,0.));
#8509=DIRECTION('center_axis',(0.,1.,0.));
#8510=DIRECTION('ref_axis',(1.,0.,0.));
#8511=DIRECTION('',(0.,-1.,0.));
#8512=DIRECTION('center_axis',(0.,1.,0.));
#8513=DIRECTION('ref_axis',(1.,0.,0.));
#8514=DIRECTION('center_axis',(0.,1.,0.));
#8515=DIRECTION('ref_axis',(1.,0.,0.));
#8516=DIRECTION('center_axis',(0.,1.,0.));
#8517=DIRECTION('ref_axis',(1.,0.,0.));
#10430=CARTESIAN_POINT('',(0.,0.,0.));
#10431=CARTESIAN_POINT('Origin',(2.,10.8,5.));
#10432=CARTESIAN_POINT('',(1.775,11.,5.));
#10433=CARTESIAN_POINT('Origin',(2.,11.,5.));
#10434=CARTESIAN_POINT('',(1.775,10.8,5.));
#10435=CARTESIAN_POINT('',(1.775,10.8,5.));
#10436=CARTESIAN_POINT('Origin',(2.,10.8,5.));
#10437=CARTESIAN_POINT('Origin',(2.,10.8,5.));
#10438=CARTESIAN_POINT('',(1.2,11.,5.));
#10439=CARTESIAN_POINT('Origin',(2.,11.,5.));
#10440=CARTESIAN_POINT('',(1.2,10.8,5.));
#10441=CARTESIAN_POINT('',(1.2,10.8,5.));
#10442=CARTESIAN_POINT('Origin',(2.,10.8,5.));
#10443=CARTESIAN_POINT('Origin',(2.,11.,5.));
#10444=CARTESIAN_POINT('Origin',(2.,10.8,5.));
#11674=UNCERTAINTY_MEASURE_WITH_UNIT(LENGTH_MEASURE(0.001),#11749,
'DISTANCE_ACCURACY_VALUE',
'Maximum model space distance between geometric entities at asserted c
onnectivities');
#11699=UNCERTAINTY_MEASURE_WITH_UNIT(LENGTH_MEASURE(0.001),#11749,
'DISTANCE_ACCURACY_VALUE',
'Maximum model space distance between geometric entities at asserted c
onnectivities');
#11723=(
GEOMETRIC_REPRESENTATION_CONTEXT(3)
GLOBAL_UNCERTAINTY_ASSIGNED_CONTEXT((#11674))
GLOBAL_UNIT_ASSIGNED_CONTEXT((#11749,#11751,#11752))
REPRESENTATION_CONTEXT('','3D')
);
#11748=(
GEOMETRIC_REPRESENTATION_CONTEXT(3)
GLOBAL_UNCERTAINTY_ASSIGNED_CONTEXT((#11699))
GLOBAL_UNIT_ASSIGNED_CONTEXT((#11749,#11751,#11752))
REPRESENTATION_CONTEXT('','3D')
);
#11749=(
LENGTH_UNIT()
NAMED_UNIT(*)
SI_UNIT(.CENTI.,.METRE.)
);
#11751=(
NAMED_UNIT(*)
PLANE_ANGLE_UNIT()
SI_UNIT($,.RADIAN.)
);
#11752=(
NAMED_UNIT(*)
SI_UNIT($,.STERADIAN.)
SOLID_ANGLE_UNIT()
);
#11776=SHAPE_DEFINITION_REPRESENTATION(#11824,#11947);
#11824=PRODUCT_DEFINITION_SHAPE('',$,#11996);
#11947=SHAPE_REPRESENTATION('',(#7077),#11723);
#11972=PRODUCT_DEFINITION_CONTEXT('part definition',#12118,'design');
#11996=PRODUCT_DEFINITION('Axle keeper_3','Axle keeper (3)',#12044,#11972);
#12044=PRODUCT_DEFINITION_FORMATION('',$,#12143);
#12118=APPLICATION_CONTEXT(
'Core Data for Automotive Mechanical Design Process');
#12119=PRODUCT_CONTEXT('part definition',#12118,'mechanical');
#12143=PRODUCT('Axle keeper_3','Axle keeper (3)','Axle keeper',(#12119));
#12169=PRESENTATION_STYLE_ASSIGNMENT((#12174));
#12174=SURFACE_STYLE_USAGE(.BOTH.,#12179);
#12179=SURFACE_SIDE_STYLE('',(#12184));
#12184=SURFACE_STYLE_FILL_AREA(#12189);
#12189=FILL_AREA_STYLE('CAD Library Painted - Engineering blue',(#12194));
#12194=FILL_AREA_STYLE_COLOUR('CAD Library Painted - Engineering blue',
#12199);
#12199=COLOUR_RGB('CAD Library Painted - Engineering blue',0.12156862745098,
0.356862745098039,0.6);
ENDSEC;
END-ISO-10303-21;
